ISO-10303-21;
HEADER;
/* Generated by software containing ST-Developer
 * from STEP Tools, Inc. (www.steptools.com) 
 */

FILE_DESCRIPTION(
/* description */ ('PAT-091'),
/* implementation_level */ '2;1');

FILE_NAME(
/* name */ 'Screw bearing cap (1).step',
/* time_stamp */ '2026-10-27T15:34:44-07:00',
/* author */ (''),
/* organization */ (''),
/* preprocessor_version */ 'ST-DEVELOPER v20.2',
/* originating_system */ 'Autodesk Translation Framework v15.17.0.0',
/* authorisation */ '');

FILE_SCHEMA (('AUTOMOTIVE_DESIGN { 1 0 10303 214 3 1 1 }'));
ENDSEC;

DATA;
#10=MECHANICAL_DESIGN_GEOMETRIC_PRESENTATION_REPRESENTATION('',(#976),#25100);
#756=SHAPE_REPRESENTATION_RELATIONSHIP('SRR','None',#25517,#866);
#866=ADVANCED_BREP_SHAPE_REPRESENTATION('',(#1100),#24987);
#976=STYLED_ITEM('',(#26198),#1100);
#1100=MANIFOLD_SOLID_BREP('Body1',#13253);
#1266=FACE_BOUND('',#2996,.T.);
#1267=FACE_BOUND('',#3000,.T.);
#1268=FACE_BOUND('',#3001,.T.);
#1269=FACE_BOUND('',#3002,.T.);
#1270=FACE_BOUND('',#3003,.T.);
#1271=FACE_BOUND('',#3004,.T.);
#1272=FACE_BOUND('',#3006,.T.);
#1273=FACE_BOUND('',#3007,.T.);
#1274=FACE_BOUND('',#3008,.T.);
#1275=FACE_BOUND('',#3009,.T.);
#1276=FACE_BOUND('',#3010,.T.);
#1671=PLANE('',#14720);
#1672=PLANE('',#14727);
#1673=PLANE('',#14728);
#2121=FACE_OUTER_BOUND('',#2990,.T.);
#2122=FACE_OUTER_BOUND('',#2991,.T.);
#2123=FACE_OUTER_BOUND('',#2992,.T.);
#2124=FACE_OUTER_BOUND('',#2993,.T.);
#2125=FACE_OUTER_BOUND('',#2994,.T.);
#2126=FACE_OUTER_BOUND('',#2995,.T.);
#2127=FACE_OUTER_BOUND('',#2997,.T.);
#2128=FACE_OUTER_BOUND('',#2998,.T.);
#2129=FACE_OUTER_BOUND('',#2999,.T.);
#2130=FACE_OUTER_BOUND('',#3005,.T.);
#2990=EDGE_LOOP('',(#9254,#9255,#9256,#9257));
#2991=EDGE_LOOP('',(#9258,#9259,#9260,#9261));
#2992=EDGE_LOOP('',(#9262,#9263,#9264,#9265));
#2993=EDGE_LOOP('',(#9266,#9267,#9268,#9269));
#2994=EDGE_LOOP('',(#9270,#9271,#9272,#9273));
#2995=EDGE_LOOP('',(#9274));
#2996=EDGE_LOOP('',(#9275));
#2997=EDGE_LOOP('',(#9276,#9277,#9278,#9279));
#2998=EDGE_LOOP('',(#9280,#9281,#9282,#9283));
#2999=EDGE_LOOP('',(#9284));
#3000=EDGE_LOOP('',(#9285));
#3001=EDGE_LOOP('',(#9286));
#3002=EDGE_LOOP('',(#9287));
#3003=EDGE_LOOP('',(#9288));
#3004=EDGE_LOOP('',(#9289));
#3005=EDGE_LOOP('',(#9290));
#3006=EDGE_LOOP('',(#9291));
#3007=EDGE_LOOP('',(#9292));
#3008=EDGE_LOOP('',(#9293));
#3009=EDGE_LOOP('',(#9294));
#3010=EDGE_LOOP('',(#9295));
#4211=LINE('',#21279,#4951);
#4212=LINE('',#21285,#4952);
#4213=LINE('',#21291,#4953);
#4214=LINE('',#21297,#4954);
#4215=LINE('',#21303,#4955);
#4216=LINE('',#21311,#4956);
#4217=LINE('',#21316,#4957);
#4951=VECTOR('',#16799,0.225);
#4952=VECTOR('',#16806,0.225);
#4953=VECTOR('',#16813,0.225);
#4954=VECTOR('',#16820,0.225);
#4955=VECTOR('',#16827,1.59);
#4956=VECTOR('',#16838,1.02);
#4957=VECTOR('',#16843,2.2);
#5658=CIRCLE('',#14706,0.225);
#5659=CIRCLE('',#14707,0.225);
#5660=CIRCLE('',#14709,0.225);
#5661=CIRCLE('',#14710,0.225);
#5662=CIRCLE('',#14712,0.225);
#5663=CIRCLE('',#14713,0.225);
#5664=CIRCLE('',#14715,0.225);
#5665=CIRCLE('',#14716,0.225);
#5666=CIRCLE('',#14718,1.59);
#5667=CIRCLE('',#14719,1.59);
#5668=CIRCLE('',#14721,1.02);
#5669=CIRCLE('',#14723,1.02);
#5670=CIRCLE('',#14725,2.2);
#5671=CIRCLE('',#14726,2.2);
#6477=VERTEX_POINT('',#21276);
#6478=VERTEX_POINT('',#21278);
#6479=VERTEX_POINT('',#21282);
#6480=VERTEX_POINT('',#21284);
#6481=VERTEX_POINT('',#21288);
#6482=VERTEX_POINT('',#21290);
#6483=VERTEX_POINT('',#21294);
#6484=VERTEX_POINT('',#21296);
#6485=VERTEX_POINT('',#21300);
#6486=VERTEX_POINT('',#21302);
#6487=VERTEX_POINT('',#21306);
#6488=VERTEX_POINT('',#21309);
#6489=VERTEX_POINT('',#21313);
#6490=VERTEX_POINT('',#21315);
#7562=EDGE_CURVE('',#6477,#6477,#5658,.T.);
#7563=EDGE_CURVE('',#6477,#6478,#4211,.T.);
#7564=EDGE_CURVE('',#6478,#6478,#5659,.T.);
#7565=EDGE_CURVE('',#6479,#6479,#5660,.T.);
#7566=EDGE_CURVE('',#6479,#6480,#4212,.T.);
#7567=EDGE_CURVE('',#6480,#6480,#5661,.T.);
#7568=EDGE_CURVE('',#6481,#6481,#5662,.T.);
#7569=EDGE_CURVE('',#6481,#6482,#4213,.T.);
#7570=EDGE_CURVE('',#6482,#6482,#5663,.T.);
#7571=EDGE_CURVE('',#6483,#6483,#5664,.T.);
#7572=EDGE_CURVE('',#6483,#6484,#4214,.T.);
#7573=EDGE_CURVE('',#6484,#6484,#5665,.T.);
#7574=EDGE_CURVE('',#6485,#6485,#5666,.T.);
#7575=EDGE_CURVE('',#6485,#6486,#4215,.T.);
#7576=EDGE_CURVE('',#6486,#6486,#5667,.T.);
#7577=EDGE_CURVE('',#6487,#6487,#5668,.T.);
#7578=EDGE_CURVE('',#6488,#6488,#5669,.T.);
#7579=EDGE_CURVE('',#6488,#6487,#4216,.T.);
#7580=EDGE_CURVE('',#6489,#6489,#5670,.T.);
#7581=EDGE_CURVE('',#6489,#6490,#4217,.T.);
#7582=EDGE_CURVE('',#6490,#6490,#5671,.T.);
#9254=ORIENTED_EDGE('',*,*,#7562,.F.);
#9255=ORIENTED_EDGE('',*,*,#7563,.T.);
#9256=ORIENTED_EDGE('',*,*,#7564,.F.);
#9257=ORIENTED_EDGE('',*,*,#7563,.F.);
#9258=ORIENTED_EDGE('',*,*,#7565,.F.);
#9259=ORIENTED_EDGE('',*,*,#7566,.T.);
#9260=ORIENTED_EDGE('',*,*,#7567,.F.);
#9261=ORIENTED_EDGE('',*,*,#7566,.F.);
#9262=ORIENTED_EDGE('',*,*,#7568,.F.);
#9263=ORIENTED_EDGE('',*,*,#7569,.T.);
#9264=ORIENTED_EDGE('',*,*,#7570,.F.);
#9265=ORIENTED_EDGE('',*,*,#7569,.F.);
#9266=ORIENTED_EDGE('',*,*,#7571,.F.);
#9267=ORIENTED_EDGE('',*,*,#7572,.T.);
#9268=ORIENTED_EDGE('',*,*,#7573,.F.);
#9269=ORIENTED_EDGE('',*,*,#7572,.F.);
#9270=ORIENTED_EDGE('',*,*,#7574,.F.);
#9271=ORIENTED_EDGE('',*,*,#7575,.T.);
#9272=ORIENTED_EDGE('',*,*,#7576,.T.);
#9273=ORIENTED_EDGE('',*,*,#7575,.F.);
#9274=ORIENTED_EDGE('',*,*,#7576,.F.);
#9275=ORIENTED_EDGE('',*,*,#7577,.F.);
#9276=ORIENTED_EDGE('',*,*,#7578,.F.);
#9277=ORIENTED_EDGE('',*,*,#7579,.T.);
#9278=ORIENTED_EDGE('',*,*,#7577,.T.);
#9279=ORIENTED_EDGE('',*,*,#7579,.F.);
#9280=ORIENTED_EDGE('',*,*,#7580,.F.);
#9281=ORIENTED_EDGE('',*,*,#7581,.T.);
#9282=ORIENTED_EDGE('',*,*,#7582,.T.);
#9283=ORIENTED_EDGE('',*,*,#7581,.F.);
#9284=ORIENTED_EDGE('',*,*,#7580,.T.);
#9285=ORIENTED_EDGE('',*,*,#7578,.T.);
#9286=ORIENTED_EDGE('',*,*,#7573,.T.);
#9287=ORIENTED_EDGE('',*,*,#7570,.T.);
#9288=ORIENTED_EDGE('',*,*,#7567,.T.);
#9289=ORIENTED_EDGE('',*,*,#7564,.T.);
#9290=ORIENTED_EDGE('',*,*,#7582,.F.);
#9291=ORIENTED_EDGE('',*,*,#7574,.T.);
#9292=ORIENTED_EDGE('',*,*,#7571,.T.);
#9293=ORIENTED_EDGE('',*,*,#7568,.T.);
#9294=ORIENTED_EDGE('',*,*,#7565,.T.);
#9295=ORIENTED_EDGE('',*,*,#7562,.T.);
#12101=CYLINDRICAL_SURFACE('',#14705,0.225);
#12102=CYLINDRICAL_SURFACE('',#14708,0.225);
#12103=CYLINDRICAL_SURFACE('',#14711,0.225);
#12104=CYLINDRICAL_SURFACE('',#14714,0.225);
#12105=CYLINDRICAL_SURFACE('',#14717,1.59);
#12106=CYLINDRICAL_SURFACE('',#14722,1.02);
#12107=CYLINDRICAL_SURFACE('',#14724,2.2);
#12488=ADVANCED_FACE('',(#2121),#12101,.F.);
#12489=ADVANCED_FACE('',(#2122),#12102,.F.);
#12490=ADVANCED_FACE('',(#2123),#12103,.F.);
#12491=ADVANCED_FACE('',(#2124),#12104,.F.);
#12492=ADVANCED_FACE('',(#2125),#12105,.T.);
#12493=ADVANCED_FACE('',(#2126,#1266),#1671,.F.);
#12494=ADVANCED_FACE('',(#2127),#12106,.F.);
#12495=ADVANCED_FACE('',(#2128),#12107,.T.);
#12496=ADVANCED_FACE('',(#2129,#1267,#1268,#1269,#1270,#1271),#1672,.T.);
#12497=ADVANCED_FACE('',(#2130,#1272,#1273,#1274,#1275,#1276),#1673,.F.);
#13253=CLOSED_SHELL('',(#12488,#12489,#12490,#12491,#12492,#12493,#12494,
#12495,#12496,#12497));
#14704=AXIS2_PLACEMENT_3D('',#21274,#16793,#16794);
#14705=AXIS2_PLACEMENT_3D('',#21275,#16795,#16796);
#14706=AXIS2_PLACEMENT_3D('',#21277,#16797,#16798);
#14707=AXIS2_PLACEMENT_3D('',#21280,#16800,#16801);
#14708=AXIS2_PLACEMENT_3D('',#21281,#16802,#16803);
#14709=AXIS2_PLACEMENT_3D('',#21283,#16804,#16805);
#14710=AXIS2_PLACEMENT_3D('',#21286,#16807,#16808);
#14711=AXIS2_PLACEMENT_3D('',#21287,#16809,#16810);
#14712=AXIS2_PLACEMENT_3D('',#21289,#16811,#16812);
#14713=AXIS2_PLACEMENT_3D('',#21292,#16814,#16815);
#14714=AXIS2_PLACEMENT_3D('',#21293,#16816,#16817);
#14715=AXIS2_PLACEMENT_3D('',#21295,#16818,#16819);
#14716=AXIS2_PLACEMENT_3D('',#21298,#16821,#16822);
#14717=AXIS2_PLACEMENT_3D('',#21299,#16823,#16824);
#14718=AXIS2_PLACEMENT_3D('',#21301,#16825,#16826);
#14719=AXIS2_PLACEMENT_3D('',#21304,#16828,#16829);
#14720=AXIS2_PLACEMENT_3D('',#21305,#16830,#16831);
#14721=AXIS2_PLACEMENT_3D('',#21307,#16832,#16833);
#14722=AXIS2_PLACEMENT_3D('',#21308,#16834,#16835);
#14723=AXIS2_PLACEMENT_3D('',#21310,#16836,#16837);
#14724=AXIS2_PLACEMENT_3D('',#21312,#16839,#16840);
#14725=AXIS2_PLACEMENT_3D('',#21314,#16841,#16842);
#14726=AXIS2_PLACEMENT_3D('',#21317,#16844,#16845);
#14727=AXIS2_PLACEMENT_3D('',#21318,#16846,#16847);
#14728=AXIS2_PLACEMENT_3D('',#21319,#16848,#16849);
#16793=DIRECTION('axis',(0.,0.,1.));
#16794=DIRECTION('refdir',(1.,0.,0.));
#16795=DIRECTION('center_axis',(1.,0.,0.));
#16796=DIRECTION('ref_axis',(0.,0.,-1.));
#16797=DIRECTION('center_axis',(1.,0.,0.));
#16798=DIRECTION('ref_axis',(0.,0.,-1.));
#16799=DIRECTION('',(1.,0.,0.));
#16800=DIRECTION('center_axis',(-1.,0.,0.));
#16801=DIRECTION('ref_axis',(0.,0.,-1.));
#16802=DIRECTION('center_axis',(1.,0.,0.));
#16803=DIRECTION('ref_axis',(0.,0.,-1.));
#16804=DIRECTION('center_axis',(1.,0.,0.));
#16805=DIRECTION('ref_axis',(0.,0.,-1.));
#16806=DIRECTION('',(1.,0.,0.));
#16807=DIRECTION('center_axis',(-1.,0.,0.));
#16808=DIRECTION('ref_axis',(0.,0.,-1.));
#16809=DIRECTION('center_axis',(1.,0.,0.));
#16810=DIRECTION('ref_axis',(0.,0.,-1.));
#16811=DIRECTION('center_axis',(1.,0.,0.));
#16812=DIRECTION('ref_axis',(0.,0.,-1.));
#16813=DIRECTION('',(1.,0.,0.));
#16814=DIRECTION('center_axis',(-1.,0.,0.));
#16815=DIRECTION('ref_axis',(0.,0.,-1.));
#16816=DIRECTION('center_axis',(1.,0.,0.));
#16817=DIRECTION('ref_axis',(0.,0.,-1.));
#16818=DIRECTION('center_axis',(1.,0.,0.));
#16819=DIRECTION('ref_axis',(0.,0.,-1.));
#16820=DIRECTION('',(1.,0.,0.));
#16821=DIRECTION('center_axis',(-1.,0.,0.));
#16822=DIRECTION('ref_axis',(0.,0.,-1.));
#16823=DIRECTION('center_axis',(1.,0.,0.));
#16824=DIRECTION('ref_axis',(0.,0.,-1.));
#16825=DIRECTION('center_axis',(1.,0.,0.));
#16826=DIRECTION('ref_axis',(0.,0.,-1.));
#16827=DIRECTION('',(-1.,0.,0.));
#16828=DIRECTION('center_axis',(1.,0.,0.));
#16829=DIRECTION('ref_axis',(0.,0.,-1.));
#16830=DIRECTION('center_axis',(1.,0.,0.));
#16831=DIRECTION('ref_axis',(0.,0.,-1.));
#16832=DIRECTION('center_axis',(-1.,0.,0.));
#16833=DIRECTION('ref_axis',(0.,0.,-1.));
#16834=DIRECTION('center_axis',(1.,0.,0.));
#16835=DIRECTION('ref_axis',(0.,0.,-1.));
#16836=DIRECTION('center_axis',(-1.,0.,0.));
#16837=DIRECTION('ref_axis',(0.,0.,-1.));
#16838=DIRECTION('',(-1.,0.,0.));
#16839=DIRECTION('center_axis',(1.,0.,0.));
#16840=DIRECTION('ref_axis',(0.,0.,-1.));
#16841=DIRECTION('center_axis',(1.,0.,0.));
#16842=DIRECTION('ref_axis',(0.,0.,-1.));
#16843=DIRECTION('',(-1.,0.,0.));
#16844=DIRECTION('center_axis',(1.,0.,0.));
#16845=DIRECTION('ref_axis',(0.,0.,-1.));
#16846=DIRECTION('center_axis',(1.,0.,0.));
#16847=DIRECTION('ref_axis',(0.,0.,-1.));
#16848=DIRECTION('center_axis',(1.,0.,0.));
#16849=DIRECTION('ref_axis',(0.,0.,-1.));
#21274=CARTESIAN_POINT('',(0.,0.,0.));
#21275=CARTESIAN_POINT('Origin',(0.9,-1.30814754519511,4.69185245480489));
#21276=CARTESIAN_POINT('',(1.,-1.30814754519511,4.91685245480489));
#21277=CARTESIAN_POINT('Origin',(1.,-1.30814754519511,4.69185245480489));
#21278=CARTESIAN_POINT('',(1.3,-1.30814754519511,4.91685245480489));
#21279=CARTESIAN_POINT('',(0.9,-1.30814754519511,4.91685245480489));
#21280=CARTESIAN_POINT('Origin',(1.3,-1.30814754519511,4.69185245480489));
#21281=CARTESIAN_POINT('Origin',(0.9,-1.30814754519511,7.30814754519511));
#21282=CARTESIAN_POINT('',(1.,-1.30814754519511,7.53314754519511));
#21283=CARTESIAN_POINT('Origin',(1.,-1.30814754519511,7.30814754519511));
#21284=CARTESIAN_POINT('',(1.3,-1.30814754519511,7.53314754519511));
#21285=CARTESIAN_POINT('',(0.9,-1.30814754519511,7.53314754519511));
#21286=CARTESIAN_POINT('Origin',(1.3,-1.30814754519511,7.30814754519511));
#21287=CARTESIAN_POINT('Origin',(0.9,1.30814754519511,7.30814754519511));
#21288=CARTESIAN_POINT('',(1.,1.30814754519511,7.53314754519511));
#21289=CARTESIAN_POINT('Origin',(1.,1.30814754519511,7.30814754519511));
#21290=CARTESIAN_POINT('',(1.3,1.30814754519511,7.53314754519511));
#21291=CARTESIAN_POINT('',(0.9,1.30814754519511,7.53314754519511));
#21292=CARTESIAN_POINT('Origin',(1.3,1.30814754519511,7.30814754519511));
#21293=CARTESIAN_POINT('Origin',(0.9,1.30814754519511,4.69185245480489));
#21294=CARTESIAN_POINT('',(1.,1.30814754519511,4.91685245480489));
#21295=CARTESIAN_POINT('Origin',(1.,1.30814754519511,4.69185245480489));
#21296=CARTESIAN_POINT('',(1.3,1.30814754519511,4.91685245480489));
#21297=CARTESIAN_POINT('',(0.9,1.30814754519511,4.91685245480489));
#21298=CARTESIAN_POINT('Origin',(1.3,1.30814754519511,4.69185245480489));
#21299=CARTESIAN_POINT('Origin',(0.5,0.,6.));
#21300=CARTESIAN_POINT('',(1.,-1.94718841064429E-16,7.59));
#21301=CARTESIAN_POINT('Origin',(1.,0.,6.));
#21302=CARTESIAN_POINT('',(0.5,-1.94718841064429E-16,7.59));
#21303=CARTESIAN_POINT('',(0.5,-1.94718841064429E-16,7.59));
#21304=CARTESIAN_POINT('Origin',(0.5,0.,6.));
#21305=CARTESIAN_POINT('Origin',(0.5,0.,6.));
#21306=CARTESIAN_POINT('',(0.5,-1.2491397351303E-16,7.02));
#21307=CARTESIAN_POINT('Origin',(0.5,0.,6.));
#21308=CARTESIAN_POINT('Origin',(1.,0.,6.));
#21309=CARTESIAN_POINT('',(1.3,-1.2491397351303E-16,7.02));
#21310=CARTESIAN_POINT('Origin',(1.3,0.,6.));
#21311=CARTESIAN_POINT('',(1.,-1.2491397351303E-16,7.02));
#21312=CARTESIAN_POINT('Origin',(1.,0.,6.));
#21313=CARTESIAN_POINT('',(1.3,-2.69422295812418E-16,8.2));
#21314=CARTESIAN_POINT('Origin',(1.3,0.,6.));
#21315=CARTESIAN_POINT('',(1.,-2.69422295812418E-16,8.2));
#21316=CARTESIAN_POINT('',(1.,-2.69422295812418E-16,8.2));
#21317=CARTESIAN_POINT('Origin',(1.,0.,6.));
#21318=CARTESIAN_POINT('Origin',(1.3,0.,6.));
#21319=CARTESIAN_POINT('Origin',(1.,0.,6.));
#24866=UNCERTAINTY_MEASURE_WITH_UNIT(LENGTH_MEASURE(0.001),#25101,
'DISTANCE_ACCURACY_VALUE',
'Maximum model space distance between geometric entities at asserted c
onnectivities');
#24979=UNCERTAINTY_MEASURE_WITH_UNIT(LENGTH_MEASURE(0.001),#25101,
'DISTANCE_ACCURACY_VALUE',
'Maximum model space distance between geometric entities at asserted c
onnectivities');
#24987=(
GEOMETRIC_REPRESENTATION_CONTEXT(3)
GLOBAL_UNCERTAINTY_ASSIGNED_CONTEXT((#24866))
GLOBAL_UNIT_ASSIGNED_CONTEXT((#25101,#25103,#25104))
REPRESENTATION_CONTEXT('','3D')
);
#25100=(
GEOMETRIC_REPRESENTATION_CONTEXT(3)
GLOBAL_UNCERTAINTY_ASSIGNED_CONTEXT((#24979))
GLOBAL_UNIT_ASSIGNED_CONTEXT((#25101,#25103,#25104))
REPRESENTATION_CONTEXT('','3D')
);
#25101=(
LENGTH_UNIT()
NAMED_UNIT(*)
SI_UNIT(.CENTI.,.METRE.)
);
#25103=(
NAMED_UNIT(*)
PLANE_ANGLE_UNIT()
SI_UNIT($,.RADIAN.)
);
#25104=(
NAMED_UNIT(*)
SI_UNIT($,.STERADIAN.)
SOLID_ANGLE_UNIT()
);
#25112=SHAPE_DEFINITION_REPRESENTATION(#25232,#25517);
#25232=PRODUCT_DEFINITION_SHAPE('',$,#25638);
#25517=SHAPE_REPRESENTATION('',(#14704),#24987);
#25630=PRODUCT_DEFINITION_CONTEXT('part definition',#25992,'design');
#25638=PRODUCT_DEFINITION('Screw bearing cap (1)','Screw bearing cap (1)',
#25758,#25630);
#25758=PRODUCT_DEFINITION_FORMATION('',$,#26001);
#25992=APPLICATION_CONTEXT(
'Core Data for Automotive Mechanical Design Process');
#25993=PRODUCT_CONTEXT('part definition',#25992,'mechanical');
#26001=PRODUCT('Screw bearing cap (1)','Screw bearing cap (1)',
'Screw bearing cap (1)',(#25993));
#26192=COLOUR_RGB('Black',0.12,0.14,0.17);
#26193=FILL_AREA_STYLE_COLOUR('',#26192);
#26194=FILL_AREA_STYLE('',(#26193));
#26195=SURFACE_STYLE_FILL_AREA(#26194);
#26196=SURFACE_SIDE_STYLE('',(#26195));
#26197=SURFACE_STYLE_USAGE(.BOTH.,#26196);
#26198=PRESENTATION_STYLE_ASSIGNMENT((#26197));
ENDSEC;
END-ISO-10303-21;
